ISO-10303-21;
HEADER;
/* Generated by software containing ST-Developer
 * from STEP Tools, Inc. (www.steptools.com) 
 */

FILE_DESCRIPTION(
/* description */ ('Spring compression tester'),
/* implementation_level */ '2;1');

FILE_NAME(
/* name */ 'Captive slot nut.step',
/* time_stamp */ '2026-10-28T03:24:11-07:00',
/* author */ (''),
/* organization */ (''),
/* preprocessor_version */ 'ST-DEVELOPER v20.2',
/* originating_system */ 'Autodesk Translation Framework v15.17.0.0',
/* authorisation */ '');

FILE_SCHEMA (('AUTOMOTIVE_DESIGN { 1 0 10303 214 3 1 1 }'));
ENDSEC;

DATA;
#10=MECHANICAL_DESIGN_GEOMETRIC_PRESENTATION_REPRESENTATION('',(#1156),#43521);
#15=ELLIPSE('',#20393,0.299389011154384,0.2117);
#16=ELLIPSE('',#20397,0.299389011154384,0.2117);
#1021=SHAPE_REPRESENTATION_RELATIONSHIP('SRR','None',#43835,#1081);
#1081=ADVANCED_BREP_SHAPE_REPRESENTATION('',(#1227),#43495);
#1156=STYLED_ITEM('',(#44209),#1227);
#1227=MANIFOLD_SOLID_BREP('Body1',#18597);
#1474=FACE_BOUND('',#4070,.T.);
#2001=PLANE('',#20383);
#2002=PLANE('',#20384);
#2003=PLANE('',#20385);
#2004=PLANE('',#20387);
#2005=PLANE('',#20388);
#2006=PLANE('',#20389);
#2007=PLANE('',#20390);
#2008=PLANE('',#20391);
#2009=PLANE('',#20392);
#2010=PLANE('',#20399);
#2011=PLANE('',#20400);
#2012=PLANE('',#20401);
#2013=PLANE('',#20402);
#2793=FACE_OUTER_BOUND('',#4067,.T.);
#2794=FACE_OUTER_BOUND('',#4068,.T.);
#2795=FACE_OUTER_BOUND('',#4069,.T.);
#2796=FACE_OUTER_BOUND('',#4071,.T.);
#2797=FACE_OUTER_BOUND('',#4072,.T.);
#2798=FACE_OUTER_BOUND('',#4073,.T.);
#2799=FACE_OUTER_BOUND('',#4074,.T.);
#2800=FACE_OUTER_BOUND('',#4075,.T.);
#2801=FACE_OUTER_BOUND('',#4076,.T.);
#2802=FACE_OUTER_BOUND('',#4077,.T.);
#2803=FACE_OUTER_BOUND('',#4078,.T.);
#2804=FACE_OUTER_BOUND('',#4079,.T.);
#2805=FACE_OUTER_BOUND('',#4080,.T.);
#2806=FACE_OUTER_BOUND('',#4081,.T.);
#4067=EDGE_LOOP('',(#14991,#14992,#14993,#14994));
#4068=EDGE_LOOP('',(#14995,#14996,#14997,#14998));
#4069=EDGE_LOOP('',(#14999,#15000,#15001,#15002));
#4070=EDGE_LOOP('',(#15003));
#4071=EDGE_LOOP('',(#15004,#15005,#15006,#15007,#15008,#15009,#15010,#15011,
#15012,#15013));
#4072=EDGE_LOOP('',(#15014,#15015,#15016,#15017));
#4073=EDGE_LOOP('',(#15018,#15019,#15020,#15021));
#4074=EDGE_LOOP('',(#15022,#15023,#15024,#15025,#15026,#15027,#15028,#15029,
#15030,#15031));
#4075=EDGE_LOOP('',(#15032,#15033,#15034,#15035));
#4076=EDGE_LOOP('',(#15036,#15037,#15038,#15039,#15040,#15041));
#4077=EDGE_LOOP('',(#15042,#15043,#15044,#15045,#15046,#15047,#15048,#15049));
#4078=EDGE_LOOP('',(#15050,#15051,#15052,#15053,#15054));
#4079=EDGE_LOOP('',(#15055,#15056,#15057,#15058));
#4080=EDGE_LOOP('',(#15059,#15060,#15061,#15062,#15063,#15064));
#4081=EDGE_LOOP('',(#15065,#15066,#15067,#15068));
#5537=LINE('',#30086,#6969);
#5538=LINE('',#30088,#6970);
#5539=LINE('',#30090,#6971);
#5540=LINE('',#30091,#6972);
#5541=LINE('',#30094,#6973);
#5542=LINE('',#30096,#6974);
#5543=LINE('',#30097,#6975);
#5544=LINE('',#30100,#6976);
#5545=LINE('',#30102,#6977);
#5546=LINE('',#30103,#6978);
#5547=LINE('',#30108,#6979);
#5548=LINE('',#30110,#6980);
#5549=LINE('',#30112,#6981);
#5550=LINE('',#30114,#6982);
#5551=LINE('',#30116,#6983);
#5552=LINE('',#30118,#6984);
#5553=LINE('',#30119,#6985);
#5554=LINE('',#30122,#6986);
#5555=LINE('',#30123,#6987);
#5556=LINE('',#30126,#6988);
#5557=LINE('',#30127,#6989);
#5558=LINE('',#30130,#6990);
#5559=LINE('',#30132,#6991);
#5560=LINE('',#30134,#6992);
#5561=LINE('',#30136,#6993);
#5562=LINE('',#30137,#6994);
#5563=LINE('',#30139,#6995);
#5564=LINE('',#30142,#6996);
#5565=LINE('',#30145,#6997);
#5566=LINE('',#30149,#6998);
#5567=LINE('',#30156,#6999);
#5568=LINE('',#30158,#7000);
#5569=LINE('',#30160,#7001);
#6969=VECTOR('',#24327,1.);
#6970=VECTOR('',#24328,1.);
#6971=VECTOR('',#24329,1.);
#6972=VECTOR('',#24330,1.);
#6973=VECTOR('',#24333,1.);
#6974=VECTOR('',#24334,1.);
#6975=VECTOR('',#24335,1.);
#6976=VECTOR('',#24338,1.);
#6977=VECTOR('',#24339,1.);
#6978=VECTOR('',#24340,1.);
#6979=VECTOR('',#24345,1.);
#6980=VECTOR('',#24346,1.);
#6981=VECTOR('',#24347,1.);
#6982=VECTOR('',#24348,1.);
#6983=VECTOR('',#24349,1.);
#6984=VECTOR('',#24350,1.);
#6985=VECTOR('',#24351,1.);
#6986=VECTOR('',#24354,1.);
#6987=VECTOR('',#24355,1.);
#6988=VECTOR('',#24358,1.);
#6989=VECTOR('',#24359,1.);
#6990=VECTOR('',#24362,1.);
#6991=VECTOR('',#24363,1.);
#6992=VECTOR('',#24364,1.);
#6993=VECTOR('',#24365,1.);
#6994=VECTOR('',#24366,1.);
#6995=VECTOR('',#24369,1.);
#6996=VECTOR('',#24372,1.);
#6997=VECTOR('',#24375,1.);
#6998=VECTOR('',#24380,0.21);
#6999=VECTOR('',#24389,1.);
#7000=VECTOR('',#24392,1.);
#7001=VECTOR('',#24395,1.);
#7894=CIRCLE('',#20386,0.2117);
#7895=CIRCLE('',#20395,0.2117);
#7896=CIRCLE('',#20396,0.2117);
#7897=CIRCLE('',#20398,0.2117);
#9073=VERTEX_POINT('',#30084);
#9074=VERTEX_POINT('',#30085);
#9075=VERTEX_POINT('',#30087);
#9076=VERTEX_POINT('',#30089);
#9077=VERTEX_POINT('',#30093);
#9078=VERTEX_POINT('',#30095);
#9079=VERTEX_POINT('',#30099);
#9080=VERTEX_POINT('',#30101);
#9081=VERTEX_POINT('',#30104);
#9082=VERTEX_POINT('',#30107);
#9083=VERTEX_POINT('',#30109);
#9084=VERTEX_POINT('',#30111);
#9085=VERTEX_POINT('',#30113);
#9086=VERTEX_POINT('',#30115);
#9087=VERTEX_POINT('',#30117);
#9088=VERTEX_POINT('',#30121);
#9089=VERTEX_POINT('',#30125);
#9090=VERTEX_POINT('',#30129);
#9091=VERTEX_POINT('',#30131);
#9092=VERTEX_POINT('',#30133);
#9093=VERTEX_POINT('',#30135);
#9094=VERTEX_POINT('',#30141);
#9095=VERTEX_POINT('',#30143);
#9096=VERTEX_POINT('',#30147);
#9097=VERTEX_POINT('',#30150);
#9098=VERTEX_POINT('',#30152);
#11160=EDGE_CURVE('',#9073,#9074,#5537,.T.);
#11161=EDGE_CURVE('',#9075,#9073,#5538,.T.);
#11162=EDGE_CURVE('',#9076,#9075,#5539,.T.);
#11163=EDGE_CURVE('',#9074,#9076,#5540,.T.);
#11164=EDGE_CURVE('',#9075,#9077,#5541,.T.);
#11165=EDGE_CURVE('',#9078,#9077,#5542,.T.);
#11166=EDGE_CURVE('',#9076,#9078,#5543,.T.);
#11167=EDGE_CURVE('',#9077,#9079,#5544,.T.);
#11168=EDGE_CURVE('',#9079,#9080,#5545,.T.);
#11169=EDGE_CURVE('',#9080,#9078,#5546,.T.);
#11170=EDGE_CURVE('',#9081,#9081,#7894,.T.);
#11171=EDGE_CURVE('',#9082,#9073,#5547,.T.);
#11172=EDGE_CURVE('',#9083,#9082,#5548,.T.);
#11173=EDGE_CURVE('',#9083,#9084,#5549,.T.);
#11174=EDGE_CURVE('',#9085,#9084,#5550,.T.);
#11175=EDGE_CURVE('',#9085,#9086,#5551,.T.);
#11176=EDGE_CURVE('',#9086,#9087,#5552,.T.);
#11177=EDGE_CURVE('',#9087,#9079,#5553,.T.);
#11178=EDGE_CURVE('',#9087,#9088,#5554,.T.);
#11179=EDGE_CURVE('',#9088,#9080,#5555,.T.);
#11180=EDGE_CURVE('',#9089,#9086,#5556,.T.);
#11181=EDGE_CURVE('',#9088,#9089,#5557,.T.);
#11182=EDGE_CURVE('',#9090,#9089,#5558,.T.);
#11183=EDGE_CURVE('',#9091,#9090,#5559,.T.);
#11184=EDGE_CURVE('',#9091,#9092,#5560,.T.);
#11185=EDGE_CURVE('',#9093,#9092,#5561,.T.);
#11186=EDGE_CURVE('',#9093,#9074,#5562,.T.);
#11187=EDGE_CURVE('',#9090,#9085,#5563,.T.);
#11188=EDGE_CURVE('',#9084,#9094,#5564,.T.);
#11189=EDGE_CURVE('',#9094,#9095,#15,.T.);
#11190=EDGE_CURVE('',#9095,#9091,#5565,.T.);
#11191=EDGE_CURVE('',#9096,#9094,#7895,.F.);
#11192=EDGE_CURVE('',#9096,#9081,#5566,.T.);
#11193=EDGE_CURVE('',#9097,#9096,#7896,.F.);
#11194=EDGE_CURVE('',#9098,#9097,#16,.T.);
#11195=EDGE_CURVE('',#9095,#9098,#7897,.F.);
#11196=EDGE_CURVE('',#9097,#9083,#5567,.T.);
#11197=EDGE_CURVE('',#9092,#9098,#5568,.T.);
#11198=EDGE_CURVE('',#9082,#9093,#5569,.T.);
#14991=ORIENTED_EDGE('',*,*,#11160,.F.);
#14992=ORIENTED_EDGE('',*,*,#11161,.F.);
#14993=ORIENTED_EDGE('',*,*,#11162,.F.);
#14994=ORIENTED_EDGE('',*,*,#11163,.F.);
#14995=ORIENTED_EDGE('',*,*,#11162,.T.);
#14996=ORIENTED_EDGE('',*,*,#11164,.T.);
#14997=ORIENTED_EDGE('',*,*,#11165,.F.);
#14998=ORIENTED_EDGE('',*,*,#11166,.F.);
#14999=ORIENTED_EDGE('',*,*,#11167,.T.);
#15000=ORIENTED_EDGE('',*,*,#11168,.T.);
#15001=ORIENTED_EDGE('',*,*,#11169,.T.);
#15002=ORIENTED_EDGE('',*,*,#11165,.T.);
#15003=ORIENTED_EDGE('',*,*,#11170,.T.);
#15004=ORIENTED_EDGE('',*,*,#11167,.F.);
#15005=ORIENTED_EDGE('',*,*,#11164,.F.);
#15006=ORIENTED_EDGE('',*,*,#11161,.T.);
#15007=ORIENTED_EDGE('',*,*,#11171,.F.);
#15008=ORIENTED_EDGE('',*,*,#11172,.F.);
#15009=ORIENTED_EDGE('',*,*,#11173,.T.);
#15010=ORIENTED_EDGE('',*,*,#11174,.F.);
#15011=ORIENTED_EDGE('',*,*,#11175,.T.);
#15012=ORIENTED_EDGE('',*,*,#11176,.T.);
#15013=ORIENTED_EDGE('',*,*,#11177,.T.);
#15014=ORIENTED_EDGE('',*,*,#11178,.T.);
#15015=ORIENTED_EDGE('',*,*,#11179,.T.);
#15016=ORIENTED_EDGE('',*,*,#11168,.F.);
#15017=ORIENTED_EDGE('',*,*,#11177,.F.);
#15018=ORIENTED_EDGE('',*,*,#11180,.F.);
#15019=ORIENTED_EDGE('',*,*,#11181,.F.);
#15020=ORIENTED_EDGE('',*,*,#11178,.F.);
#15021=ORIENTED_EDGE('',*,*,#11176,.F.);
#15022=ORIENTED_EDGE('',*,*,#11169,.F.);
#15023=ORIENTED_EDGE('',*,*,#11179,.F.);
#15024=ORIENTED_EDGE('',*,*,#11181,.T.);
#15025=ORIENTED_EDGE('',*,*,#11182,.F.);
#15026=ORIENTED_EDGE('',*,*,#11183,.F.);
#15027=ORIENTED_EDGE('',*,*,#11184,.T.);
#15028=ORIENTED_EDGE('',*,*,#11185,.F.);
#15029=ORIENTED_EDGE('',*,*,#11186,.T.);
#15030=ORIENTED_EDGE('',*,*,#11163,.T.);
#15031=ORIENTED_EDGE('',*,*,#11166,.T.);
#15032=ORIENTED_EDGE('',*,*,#11180,.T.);
#15033=ORIENTED_EDGE('',*,*,#11175,.F.);
#15034=ORIENTED_EDGE('',*,*,#11187,.F.);
#15035=ORIENTED_EDGE('',*,*,#11182,.T.);
#15036=ORIENTED_EDGE('',*,*,#11183,.T.);
#15037=ORIENTED_EDGE('',*,*,#11187,.T.);
#15038=ORIENTED_EDGE('',*,*,#11174,.T.);
#15039=ORIENTED_EDGE('',*,*,#11188,.T.);
#15040=ORIENTED_EDGE('',*,*,#11189,.T.);
#15041=ORIENTED_EDGE('',*,*,#11190,.T.);
#15042=ORIENTED_EDGE('',*,*,#11189,.F.);
#15043=ORIENTED_EDGE('',*,*,#11191,.F.);
#15044=ORIENTED_EDGE('',*,*,#11192,.T.);
#15045=ORIENTED_EDGE('',*,*,#11170,.F.);
#15046=ORIENTED_EDGE('',*,*,#11192,.F.);
#15047=ORIENTED_EDGE('',*,*,#11193,.F.);
#15048=ORIENTED_EDGE('',*,*,#11194,.F.);
#15049=ORIENTED_EDGE('',*,*,#11195,.F.);
#15050=ORIENTED_EDGE('',*,*,#11188,.F.);
#15051=ORIENTED_EDGE('',*,*,#11173,.F.);
#15052=ORIENTED_EDGE('',*,*,#11196,.F.);
#15053=ORIENTED_EDGE('',*,*,#11193,.T.);
#15054=ORIENTED_EDGE('',*,*,#11191,.T.);
#15055=ORIENTED_EDGE('',*,*,#11190,.F.);
#15056=ORIENTED_EDGE('',*,*,#11195,.T.);
#15057=ORIENTED_EDGE('',*,*,#11197,.F.);
#15058=ORIENTED_EDGE('',*,*,#11184,.F.);
#15059=ORIENTED_EDGE('',*,*,#11172,.T.);
#15060=ORIENTED_EDGE('',*,*,#11198,.T.);
#15061=ORIENTED_EDGE('',*,*,#11185,.T.);
#15062=ORIENTED_EDGE('',*,*,#11197,.T.);
#15063=ORIENTED_EDGE('',*,*,#11194,.T.);
#15064=ORIENTED_EDGE('',*,*,#11196,.T.);
#15065=ORIENTED_EDGE('',*,*,#11160,.T.);
#15066=ORIENTED_EDGE('',*,*,#11186,.F.);
#15067=ORIENTED_EDGE('',*,*,#11198,.F.);
#15068=ORIENTED_EDGE('',*,*,#11171,.T.);
#17259=CYLINDRICAL_SURFACE('',#20394,0.2117);
#18117=ADVANCED_FACE('',(#2793),#2001,.F.);
#18118=ADVANCED_FACE('',(#2794),#2002,.T.);
#18119=ADVANCED_FACE('',(#2795,#1474),#2003,.T.);
#18120=ADVANCED_FACE('',(#2796),#2004,.T.);
#18121=ADVANCED_FACE('',(#2797),#2005,.T.);
#18122=ADVANCED_FACE('',(#2798),#2006,.F.);
#18123=ADVANCED_FACE('',(#2799),#2007,.T.);
#18124=ADVANCED_FACE('',(#2800),#2008,.T.);
#18125=ADVANCED_FACE('',(#2801),#2009,.T.);
#18126=ADVANCED_FACE('',(#2802),#17259,.F.);
#18127=ADVANCED_FACE('',(#2803),#2010,.F.);
#18128=ADVANCED_FACE('',(#2804),#2011,.F.);
#18129=ADVANCED_FACE('',(#2805),#2012,.T.);
#18130=ADVANCED_FACE('',(#2806),#2013,.T.);
#18597=CLOSED_SHELL('',(#18117,#18118,#18119,#18120,#18121,#18122,#18123,
#18124,#18125,#18126,#18127,#18128,#18129,#18130));
#20382=AXIS2_PLACEMENT_3D('',#30082,#24323,#24324);
#20383=AXIS2_PLACEMENT_3D('',#30083,#24325,#24326);
#20384=AXIS2_PLACEMENT_3D('',#30092,#24331,#24332);
#20385=AXIS2_PLACEMENT_3D('',#30098,#24336,#24337);
#20386=AXIS2_PLACEMENT_3D('',#30105,#24341,#24342);
#20387=AXIS2_PLACEMENT_3D('',#30106,#24343,#24344);
#20388=AXIS2_PLACEMENT_3D('',#30120,#24352,#24353);
#20389=AXIS2_PLACEMENT_3D('',#30124,#24356,#24357);
#20390=AXIS2_PLACEMENT_3D('',#30128,#24360,#24361);
#20391=AXIS2_PLACEMENT_3D('',#30138,#24367,#24368);
#20392=AXIS2_PLACEMENT_3D('',#30140,#24370,#24371);
#20393=AXIS2_PLACEMENT_3D('',#30144,#24373,#24374);
#20394=AXIS2_PLACEMENT_3D('',#30146,#24376,#24377);
#20395=AXIS2_PLACEMENT_3D('',#30148,#24378,#24379);
#20396=AXIS2_PLACEMENT_3D('',#30151,#24381,#24382);
#20397=AXIS2_PLACEMENT_3D('',#30153,#24383,#24384);
#20398=AXIS2_PLACEMENT_3D('',#30154,#24385,#24386);
#20399=AXIS2_PLACEMENT_3D('',#30155,#24387,#24388);
#20400=AXIS2_PLACEMENT_3D('',#30157,#24390,#24391);
#20401=AXIS2_PLACEMENT_3D('',#30159,#24393,#24394);
#20402=AXIS2_PLACEMENT_3D('',#30161,#24396,#24397);
#24323=DIRECTION('axis',(0.,0.,1.));
#24324=DIRECTION('refdir',(1.,0.,0.));
#24325=DIRECTION('center_axis',(0.,0.,1.));
#24326=DIRECTION('ref_axis',(1.,0.,0.));
#24327=DIRECTION('',(1.,0.,0.));
#24328=DIRECTION('',(0.,-1.,0.));
#24329=DIRECTION('',(-1.,0.,0.));
#24330=DIRECTION('',(0.,1.,0.));
#24331=DIRECTION('center_axis',(0.,1.,0.));
#24332=DIRECTION('ref_axis',(-1.,0.,0.));
#24333=DIRECTION('',(0.,0.,1.));
#24334=DIRECTION('',(-1.,0.,0.));
#24335=DIRECTION('',(0.,0.,1.));
#24336=DIRECTION('center_axis',(0.,0.,1.));
#24337=DIRECTION('ref_axis',(1.,0.,0.));
#24338=DIRECTION('',(0.,-1.,0.));
#24339=DIRECTION('',(1.,0.,0.));
#24340=DIRECTION('',(0.,1.,0.));
#24341=DIRECTION('center_axis',(0.,0.,-1.));
#24342=DIRECTION('ref_axis',(1.,0.,0.));
#24343=DIRECTION('center_axis',(-1.,0.,0.));
#24344=DIRECTION('ref_axis',(0.,-1.,0.));
#24345=DIRECTION('',(0.,0.,1.));
#24346=DIRECTION('',(0.,0.707106781186548,0.707106781186548));
#24347=DIRECTION('',(0.,-1.,0.));
#24348=DIRECTION('',(0.,0.707106781186548,-0.707106781186548));
#24349=DIRECTION('',(0.,0.,1.));
#24350=DIRECTION('',(0.,-1.,0.));
#24351=DIRECTION('',(0.,0.,1.));
#24352=DIRECTION('center_axis',(0.,-1.,0.));
#24353=DIRECTION('ref_axis',(1.,0.,0.));
#24354=DIRECTION('',(1.,0.,0.));
#24355=DIRECTION('',(0.,0.,1.));
#24356=DIRECTION('center_axis',(0.,0.,1.));
#24357=DIRECTION('ref_axis',(1.,0.,0.));
#24358=DIRECTION('',(-1.,0.,0.));
#24359=DIRECTION('',(0.,1.,0.));
#24360=DIRECTION('center_axis',(1.,0.,0.));
#24361=DIRECTION('ref_axis',(0.,1.,0.));
#24362=DIRECTION('',(0.,0.,1.));
#24363=DIRECTION('',(0.,-0.707106781186548,0.707106781186548));
#24364=DIRECTION('',(0.,1.,0.));
#24365=DIRECTION('',(0.,-0.707106781186548,-0.707106781186548));
#24366=DIRECTION('',(0.,0.,1.));
#24367=DIRECTION('center_axis',(0.,-1.,0.));
#24368=DIRECTION('ref_axis',(1.,0.,0.));
#24369=DIRECTION('',(-1.,0.,0.));
#24370=DIRECTION('center_axis',(0.,-0.707106781186548,-0.707106781186548));
#24371=DIRECTION('ref_axis',(-1.,0.,0.));
#24372=DIRECTION('',(1.,0.,0.));
#24373=DIRECTION('center_axis',(0.,0.707106781186548,0.707106781186548));
#24374=DIRECTION('ref_axis',(0.,0.707106781186547,-0.707106781186547));
#24375=DIRECTION('',(1.,0.,0.));
#24376=DIRECTION('center_axis',(0.,0.,1.));
#24377=DIRECTION('ref_axis',(1.,0.,0.));
#24378=DIRECTION('center_axis',(0.,0.,-1.));
#24379=DIRECTION('ref_axis',(1.,0.,0.));
#24380=DIRECTION('',(0.,0.,1.));
#24381=DIRECTION('center_axis',(0.,0.,-1.));
#24382=DIRECTION('ref_axis',(1.,0.,0.));
#24383=DIRECTION('center_axis',(0.,-0.707106781186548,0.707106781186548));
#24384=DIRECTION('ref_axis',(0.,0.707106781186547,0.707106781186547));
#24385=DIRECTION('center_axis',(0.,0.,-1.));
#24386=DIRECTION('ref_axis',(1.,0.,0.));
#24387=DIRECTION('center_axis',(0.,0.,1.));
#24388=DIRECTION('ref_axis',(1.,0.,0.));
#24389=DIRECTION('',(-1.,0.,0.));
#24390=DIRECTION('center_axis',(0.,0.,1.));
#24391=DIRECTION('ref_axis',(1.,0.,0.));
#24392=DIRECTION('',(-1.,0.,0.));
#24393=DIRECTION('center_axis',(0.,0.707106781186548,-0.707106781186548));
#24394=DIRECTION('ref_axis',(-1.,0.,0.));
#24395=DIRECTION('',(1.,0.,0.));
#24396=DIRECTION('center_axis',(0.,1.,0.));
#24397=DIRECTION('ref_axis',(-1.,0.,0.));
#30082=CARTESIAN_POINT('',(0.,0.,0.));
#30083=CARTESIAN_POINT('Origin',(0.,0.395,0.25));
#30084=CARTESIAN_POINT('',(-0.5,0.3,0.25));
#30085=CARTESIAN_POINT('',(0.5,0.3,0.25));
#30086=CARTESIAN_POINT('',(0.25,0.3,0.25));
#30087=CARTESIAN_POINT('',(-0.5,0.5,0.25));
#30088=CARTESIAN_POINT('',(-0.5,0.5,0.25));
#30089=CARTESIAN_POINT('',(0.5,0.5,0.25));
#30090=CARTESIAN_POINT('',(0.5,0.5,0.25));
#30091=CARTESIAN_POINT('',(0.5,0.29,0.25));
#30092=CARTESIAN_POINT('Origin',(0.5,0.5,0.25));
#30093=CARTESIAN_POINT('',(-0.5,0.5,0.4));
#30094=CARTESIAN_POINT('',(-0.5,0.5,0.25));
#30095=CARTESIAN_POINT('',(0.5,0.5,0.4));
#30096=CARTESIAN_POINT('',(0.5,0.5,0.4));
#30097=CARTESIAN_POINT('',(0.5,0.5,0.25));
#30098=CARTESIAN_POINT('Origin',(0.,0.,0.4));
#30099=CARTESIAN_POINT('',(-0.5,-0.5,0.4));
#30100=CARTESIAN_POINT('',(-0.5,0.5,0.4));
#30101=CARTESIAN_POINT('',(0.5,-0.5,0.4));
#30102=CARTESIAN_POINT('',(-0.5,-0.5,0.4));
#30103=CARTESIAN_POINT('',(0.5,-0.3,0.4));
#30104=CARTESIAN_POINT('',(-0.2117,2.59257727379495E-17,0.4));
#30105=CARTESIAN_POINT('Origin',(0.,0.,0.4));
#30106=CARTESIAN_POINT('Origin',(-0.5,0.3,0.));
#30107=CARTESIAN_POINT('',(-0.5,0.3,0.15));
#30108=CARTESIAN_POINT('',(-0.5,0.3,0.));
#30109=CARTESIAN_POINT('',(-0.5,0.15,0.));
#30110=CARTESIAN_POINT('',(-0.5,0.225,0.075));
#30111=CARTESIAN_POINT('',(-0.5,-0.15,0.));
#30112=CARTESIAN_POINT('',(-0.5,0.3,0.));
#30113=CARTESIAN_POINT('',(-0.5,-0.3,0.15));
#30114=CARTESIAN_POINT('',(-0.5,-0.075,-0.075));
#30115=CARTESIAN_POINT('',(-0.5,-0.3,0.25));
#30116=CARTESIAN_POINT('',(-0.5,-0.3,0.));
#30117=CARTESIAN_POINT('',(-0.5,-0.5,0.25));
#30118=CARTESIAN_POINT('',(-0.5,-0.29,0.25));
#30119=CARTESIAN_POINT('',(-0.5,-0.5,0.25));
#30120=CARTESIAN_POINT('Origin',(-0.5,-0.5,0.25));
#30121=CARTESIAN_POINT('',(0.5,-0.5,0.25));
#30122=CARTESIAN_POINT('',(-0.5,-0.5,0.25));
#30123=CARTESIAN_POINT('',(0.5,-0.5,0.25));
#30124=CARTESIAN_POINT('Origin',(0.,-0.395,0.25));
#30125=CARTESIAN_POINT('',(0.5,-0.3,0.25));
#30126=CARTESIAN_POINT('',(-0.25,-0.3,0.25));
#30127=CARTESIAN_POINT('',(0.5,-0.5,0.25));
#30128=CARTESIAN_POINT('Origin',(0.5,-0.3,0.));
#30129=CARTESIAN_POINT('',(0.5,-0.3,0.15));
#30130=CARTESIAN_POINT('',(0.5,-0.3,0.));
#30131=CARTESIAN_POINT('',(0.5,-0.15,0.));
#30132=CARTESIAN_POINT('',(0.5,-0.225,0.075));
#30133=CARTESIAN_POINT('',(0.5,0.15,0.));
#30134=CARTESIAN_POINT('',(0.5,-0.3,0.));
#30135=CARTESIAN_POINT('',(0.5,0.3,0.15));
#30136=CARTESIAN_POINT('',(0.5,0.075,-0.075));
#30137=CARTESIAN_POINT('',(0.5,0.3,0.));
#30138=CARTESIAN_POINT('Origin',(-0.5,-0.3,0.));
#30139=CARTESIAN_POINT('',(-0.25,-0.3,0.15));
#30140=CARTESIAN_POINT('Origin',(-0.25,-0.225,0.075));
#30141=CARTESIAN_POINT('',(-0.149388386429468,-0.15,0.));
#30142=CARTESIAN_POINT('',(-0.25,-0.15,0.));
#30143=CARTESIAN_POINT('',(0.149388386429468,-0.15,0.));
#30144=CARTESIAN_POINT('Origin',(0.,0.,-0.15));
#30145=CARTESIAN_POINT('',(-0.25,-0.15,0.));
#30146=CARTESIAN_POINT('Origin',(0.,0.,-0.1));
#30147=CARTESIAN_POINT('',(-0.2117,-2.59257727379495E-17,0.));
#30148=CARTESIAN_POINT('Origin',(0.,0.,0.));
#30149=CARTESIAN_POINT('',(-0.2117,-2.59257727379495E-17,-0.1));
#30150=CARTESIAN_POINT('',(-0.149388386429468,0.15,0.));
#30151=CARTESIAN_POINT('Origin',(0.,0.,0.));
#30152=CARTESIAN_POINT('',(0.149388386429468,0.15,0.));
#30153=CARTESIAN_POINT('Origin',(0.,0.,-0.15));
#30154=CARTESIAN_POINT('Origin',(0.,0.,0.));
#30155=CARTESIAN_POINT('Origin',(0.,0.,0.));
#30156=CARTESIAN_POINT('',(0.25,0.15,0.));
#30157=CARTESIAN_POINT('Origin',(0.,0.,0.));
#30158=CARTESIAN_POINT('',(0.25,0.15,0.));
#30159=CARTESIAN_POINT('Origin',(0.25,0.225,0.075));
#30160=CARTESIAN_POINT('',(0.25,0.3,0.15));
#30161=CARTESIAN_POINT('Origin',(0.5,0.3,0.));
#43427=UNCERTAINTY_MEASURE_WITH_UNIT(LENGTH_MEASURE(0.001),#43522,
'DISTANCE_ACCURACY_VALUE',
'Maximum model space distance between geometric entities at asserted c
onnectivities');
#43453=UNCERTAINTY_MEASURE_WITH_UNIT(LENGTH_MEASURE(0.001),#43522,
'DISTANCE_ACCURACY_VALUE',
'Maximum model space distance between geometric entities at asserted c
onnectivities');
#43495=(
GEOMETRIC_REPRESENTATION_CONTEXT(3)
GLOBAL_UNCERTAINTY_ASSIGNED_CONTEXT((#43427))
GLOBAL_UNIT_ASSIGNED_CONTEXT((#43522,#43524,#43525))
REPRESENTATION_CONTEXT('','3D')
);
#43521=(
GEOMETRIC_REPRESENTATION_CONTEXT(3)
GLOBAL_UNCERTAINTY_ASSIGNED_CONTEXT((#43453))
GLOBAL_UNIT_ASSIGNED_CONTEXT((#43522,#43524,#43525))
REPRESENTATION_CONTEXT('','3D')
);
#43522=(
LENGTH_UNIT()
NAMED_UNIT(*)
SI_UNIT(.CENTI.,.METRE.)
);
#43524=(
NAMED_UNIT(*)
PLANE_ANGLE_UNIT()
SI_UNIT($,.RADIAN.)
);
#43525=(
NAMED_UNIT(*)
SI_UNIT($,.STERADIAN.)
SOLID_ANGLE_UNIT()
);
#43567=SHAPE_DEFINITION_REPRESENTATION(#43644,#43835);
#43644=PRODUCT_DEFINITION_SHAPE('',$,#43903);
#43835=SHAPE_REPRESENTATION('',(#20382),#43495);
#43861=PRODUCT_DEFINITION_CONTEXT('part definition',#44064,'design');
#43903=PRODUCT_DEFINITION('Captive slot nut','Captive slot nut',#43970,
#43861);
#43970=PRODUCT_DEFINITION_FORMATION('',$,#44107);
#44064=APPLICATION_CONTEXT(
'Core Data for Automotive Mechanical Design Process');
#44065=PRODUCT_CONTEXT('part definition',#44064,'mechanical');
#44107=PRODUCT('Captive slot nut','Captive slot nut','Captive slot nut',
(#44065));
#44203=COLOUR_RGB('Black',0.12,0.14,0.17);
#44204=FILL_AREA_STYLE_COLOUR('',#44203);
#44205=FILL_AREA_STYLE('',(#44204));
#44206=SURFACE_STYLE_FILL_AREA(#44205);
#44207=SURFACE_SIDE_STYLE('',(#44206));
#44208=SURFACE_STYLE_USAGE(.BOTH.,#44207);
#44209=PRESENTATION_STYLE_ASSIGNMENT((#44208));
ENDSEC;
END-ISO-10303-21;
